ISO-10303-21;
HEADER;
/* Generated by software containing ST-Developer
 * from STEP Tools, Inc. (www.steptools.com) 
 */

FILE_DESCRIPTION(
/* description */ ('Jaw-coupled motor to shaft test stand'),
/* implementation_level */ '2;1');

FILE_NAME(
/* name */ 'Shaft collar (1).step',
/* time_stamp */ '2026-10-27T10:46:06-07:00',
/* author */ (''),
/* organization */ (''),
/* preprocessor_version */ 'ST-DEVELOPER v20.2',
/* originating_system */ 'Autodesk Translation Framework v15.17.0.0',
/* authorisation */ '');

FILE_SCHEMA (('AUTOMOTIVE_DESIGN { 1 0 10303 214 3 1 1 }'));
ENDSEC;

DATA;
#10=MECHANICAL_DESIGN_GEOMETRIC_PRESENTATION_REPRESENTATION('',(#364),#19361);
#263=B_SPLINE_CURVE_WITH_KNOTS('',3,(#17163,#17164,#17165,#17166,#17167,
#17168,#17169,#17170,#17171,#17172),.UNSPECIFIED.,.F.,.F.,(4,2,2,2,4),(0.818088904349168,
0.878131747417163,0.957937926194034,1.03774410497091,1.0977869480389),
 .UNSPECIFIED.);
#264=B_SPLINE_CURVE_WITH_KNOTS('',3,(#17178,#17179,#17180,#17181,#17182,
#17183,#17184,#17185,#17186,#17187,#17188,#17189,#17190,#17191,#17192,#17193,
#17194,#17195),.UNSPECIFIED.,.F.,.F.,(4,2,2,2,2,2,2,2,4),(0.,0.079315764391521,
0.158631528783042,0.237943615933648,0.317255703084255,0.396567790234861,
0.475879877385467,0.555195641776988,0.634511406168509),.UNSPECIFIED.);
#265=B_SPLINE_CURVE_WITH_KNOTS('',3,(#17196,#17197,#17198,#17199,#17200,
#17201,#17202,#17203,#17204,#17205,#17206,#17207,#17208,#17209,#17210,#17211,
#17212,#17213),.UNSPECIFIED.,.F.,.F.,(4,2,2,2,2,2,2,2,4),(0.634511406168509,
0.71382717056003,0.793142934951551,0.872455022102158,0.951767109252764,
1.03107919640337,1.11039128355398,1.1897070479455,1.26902281233702),
 .UNSPECIFIED.);
#266=B_SPLINE_CURVE_WITH_KNOTS('',3,(#17216,#17217,#17218,#17219,#17220,
#17221,#17222,#17223,#17224,#17225),.UNSPECIFIED.,.F.,.F.,(4,2,2,2,4),(0.179463620219808,
0.239506463287807,0.319312642064678,0.399118820841549,0.459161663909549),
 .UNSPECIFIED.);
#299=SHAPE_REPRESENTATION_RELATIONSHIP('SRR','None',#19515,#331);
#331=ADVANCED_BREP_SHAPE_REPRESENTATION('',(#395),#19351);
#364=STYLED_ITEM('',(#19746),#395);
#395=MANIFOLD_SOLID_BREP('Body1',#11010);
#499=FACE_BOUND('',#1984,.T.);
#500=FACE_BOUND('',#1986,.T.);
#501=FACE_BOUND('',#1988,.T.);
#502=FACE_BOUND('',#1990,.T.);
#679=PLANE('',#11823);
#680=PLANE('',#11828);
#681=PLANE('',#11835);
#682=PLANE('',#11836);
#1264=FACE_OUTER_BOUND('',#1980,.T.);
#1265=FACE_OUTER_BOUND('',#1981,.T.);
#1266=FACE_OUTER_BOUND('',#1982,.T.);
#1267=FACE_OUTER_BOUND('',#1983,.T.);
#1268=FACE_OUTER_BOUND('',#1985,.T.);
#1269=FACE_OUTER_BOUND('',#1987,.T.);
#1270=FACE_OUTER_BOUND('',#1989,.T.);
#1980=EDGE_LOOP('',(#8380,#8381));
#1981=EDGE_LOOP('',(#8382,#8383,#8384,#8385,#8386,#8387,#8388,#8389,#8390));
#1982=EDGE_LOOP('',(#8391,#8392,#8393));
#1983=EDGE_LOOP('',(#8394,#8395,#8396,#8397));
#1984=EDGE_LOOP('',(#8398,#8399,#8400,#8401));
#1985=EDGE_LOOP('',(#8402,#8403,#8404,#8405));
#1986=EDGE_LOOP('',(#8406,#8407));
#1987=EDGE_LOOP('',(#8408));
#1988=EDGE_LOOP('',(#8409));
#1989=EDGE_LOOP('',(#8410));
#1990=EDGE_LOOP('',(#8411));
#2703=LINE('',#17159,#3856);
#2704=LINE('',#17176,#3857);
#2705=LINE('',#17227,#3858);
#2706=LINE('',#17232,#3859);
#2707=LINE('',#17238,#3860);
#3856=VECTOR('',#13570,1.);
#3857=VECTOR('',#13577,0.21);
#3858=VECTOR('',#13582,1.);
#3859=VECTOR('',#13587,0.605);
#3860=VECTOR('',#13594,1.1);
#4834=CIRCLE('',#11824,0.21);
#4835=CIRCLE('',#11826,0.21);
#4836=CIRCLE('',#11827,0.21);
#4837=CIRCLE('',#11830,0.605);
#4838=CIRCLE('',#11831,0.605);
#4839=CIRCLE('',#11833,1.1);
#4840=CIRCLE('',#11834,1.1);
#5294=VERTEX_POINT('',#17157);
#5295=VERTEX_POINT('',#17158);
#5296=VERTEX_POINT('',#17162);
#5297=VERTEX_POINT('',#17173);
#5298=VERTEX_POINT('',#17175);
#5299=VERTEX_POINT('',#17177);
#5300=VERTEX_POINT('',#17214);
#5301=VERTEX_POINT('',#17229);
#5302=VERTEX_POINT('',#17231);
#5303=VERTEX_POINT('',#17235);
#5304=VERTEX_POINT('',#17237);
#6401=EDGE_CURVE('',#5294,#5295,#2703,.T.);
#6402=EDGE_CURVE('',#5294,#5295,#4834,.T.);
#6403=EDGE_CURVE('',#5296,#5294,#263,.T.);
#6404=EDGE_CURVE('',#5297,#5296,#4835,.T.);
#6405=EDGE_CURVE('',#5297,#5298,#2704,.T.);
#6406=EDGE_CURVE('',#5299,#5298,#264,.T.);
#6407=EDGE_CURVE('',#5298,#5299,#265,.T.);
#6408=EDGE_CURVE('',#5300,#5297,#4836,.T.);
#6409=EDGE_CURVE('',#5295,#5300,#266,.T.);
#6410=EDGE_CURVE('',#5300,#5296,#2705,.T.);
#6411=EDGE_CURVE('',#5301,#5301,#4837,.T.);
#6412=EDGE_CURVE('',#5301,#5302,#2706,.T.);
#6413=EDGE_CURVE('',#5302,#5302,#4838,.T.);
#6414=EDGE_CURVE('',#5303,#5303,#4839,.T.);
#6415=EDGE_CURVE('',#5303,#5304,#2707,.T.);
#6416=EDGE_CURVE('',#5304,#5304,#4840,.T.);
#8380=ORIENTED_EDGE('',*,*,#6401,.F.);
#8381=ORIENTED_EDGE('',*,*,#6402,.T.);
#8382=ORIENTED_EDGE('',*,*,#6403,.F.);
#8383=ORIENTED_EDGE('',*,*,#6404,.F.);
#8384=ORIENTED_EDGE('',*,*,#6405,.T.);
#8385=ORIENTED_EDGE('',*,*,#6406,.F.);
#8386=ORIENTED_EDGE('',*,*,#6407,.F.);
#8387=ORIENTED_EDGE('',*,*,#6405,.F.);
#8388=ORIENTED_EDGE('',*,*,#6408,.F.);
#8389=ORIENTED_EDGE('',*,*,#6409,.F.);
#8390=ORIENTED_EDGE('',*,*,#6402,.F.);
#8391=ORIENTED_EDGE('',*,*,#6410,.F.);
#8392=ORIENTED_EDGE('',*,*,#6408,.T.);
#8393=ORIENTED_EDGE('',*,*,#6404,.T.);
#8394=ORIENTED_EDGE('',*,*,#6411,.F.);
#8395=ORIENTED_EDGE('',*,*,#6412,.T.);
#8396=ORIENTED_EDGE('',*,*,#6413,.T.);
#8397=ORIENTED_EDGE('',*,*,#6412,.F.);
#8398=ORIENTED_EDGE('',*,*,#6409,.T.);
#8399=ORIENTED_EDGE('',*,*,#6410,.T.);
#8400=ORIENTED_EDGE('',*,*,#6403,.T.);
#8401=ORIENTED_EDGE('',*,*,#6401,.T.);
#8402=ORIENTED_EDGE('',*,*,#6414,.F.);
#8403=ORIENTED_EDGE('',*,*,#6415,.T.);
#8404=ORIENTED_EDGE('',*,*,#6416,.T.);
#8405=ORIENTED_EDGE('',*,*,#6415,.F.);
#8406=ORIENTED_EDGE('',*,*,#6406,.T.);
#8407=ORIENTED_EDGE('',*,*,#6407,.T.);
#8408=ORIENTED_EDGE('',*,*,#6414,.T.);
#8409=ORIENTED_EDGE('',*,*,#6411,.T.);
#8410=ORIENTED_EDGE('',*,*,#6416,.F.);
#8411=ORIENTED_EDGE('',*,*,#6413,.F.);
#10341=CYLINDRICAL_SURFACE('',#11825,0.21);
#10342=CYLINDRICAL_SURFACE('',#11829,0.605);
#10343=CYLINDRICAL_SURFACE('',#11832,1.1);
#10606=ADVANCED_FACE('',(#1264),#679,.T.);
#10607=ADVANCED_FACE('',(#1265),#10341,.F.);
#10608=ADVANCED_FACE('',(#1266),#680,.T.);
#10609=ADVANCED_FACE('',(#1267,#499),#10342,.F.);
#10610=ADVANCED_FACE('',(#1268,#500),#10343,.T.);
#10611=ADVANCED_FACE('',(#1269,#501),#681,.T.);
#10612=ADVANCED_FACE('',(#1270,#502),#682,.F.);
#11010=CLOSED_SHELL('',(#10606,#10607,#10608,#10609,#10610,#10611,#10612));
#11822=AXIS2_PLACEMENT_3D('',#17155,#13566,#13567);
#11823=AXIS2_PLACEMENT_3D('',#17156,#13568,#13569);
#11824=AXIS2_PLACEMENT_3D('',#17160,#13571,#13572);
#11825=AXIS2_PLACEMENT_3D('',#17161,#13573,#13574);
#11826=AXIS2_PLACEMENT_3D('',#17174,#13575,#13576);
#11827=AXIS2_PLACEMENT_3D('',#17215,#13578,#13579);
#11828=AXIS2_PLACEMENT_3D('',#17226,#13580,#13581);
#11829=AXIS2_PLACEMENT_3D('',#17228,#13583,#13584);
#11830=AXIS2_PLACEMENT_3D('',#17230,#13585,#13586);
#11831=AXIS2_PLACEMENT_3D('',#17233,#13588,#13589);
#11832=AXIS2_PLACEMENT_3D('',#17234,#13590,#13591);
#11833=AXIS2_PLACEMENT_3D('',#17236,#13592,#13593);
#11834=AXIS2_PLACEMENT_3D('',#17239,#13595,#13596);
#11835=AXIS2_PLACEMENT_3D('',#17240,#13597,#13598);
#11836=AXIS2_PLACEMENT_3D('',#17241,#13599,#13600);
#13566=DIRECTION('axis',(0.,0.,1.));
#13567=DIRECTION('refdir',(1.,0.,0.));
#13568=DIRECTION('center_axis',(0.,0.,1.));
#13569=DIRECTION('ref_axis',(1.,0.,0.));
#13570=DIRECTION('',(0.,1.,0.));
#13571=DIRECTION('center_axis',(0.,0.,1.));
#13572=DIRECTION('ref_axis',(1.,0.,0.));
#13573=DIRECTION('center_axis',(0.,0.,1.));
#13574=DIRECTION('ref_axis',(1.,0.,0.));
#13575=DIRECTION('center_axis',(0.,0.,1.));
#13576=DIRECTION('ref_axis',(1.,0.,0.));
#13577=DIRECTION('',(0.,0.,1.));
#13578=DIRECTION('center_axis',(0.,0.,1.));
#13579=DIRECTION('ref_axis',(1.,0.,0.));
#13580=DIRECTION('center_axis',(0.,0.,1.));
#13581=DIRECTION('ref_axis',(1.,0.,0.));
#13582=DIRECTION('',(0.,-1.,0.));
#13583=DIRECTION('center_axis',(0.,1.,0.));
#13584=DIRECTION('ref_axis',(1.,0.,0.));
#13585=DIRECTION('center_axis',(0.,-1.,0.));
#13586=DIRECTION('ref_axis',(1.,0.,0.));
#13587=DIRECTION('',(0.,-1.,0.));
#13588=DIRECTION('center_axis',(0.,-1.,0.));
#13589=DIRECTION('ref_axis',(1.,0.,0.));
#13590=DIRECTION('center_axis',(0.,1.,0.));
#13591=DIRECTION('ref_axis',(1.,0.,0.));
#13592=DIRECTION('center_axis',(0.,1.,0.));
#13593=DIRECTION('ref_axis',(1.,0.,0.));
#13594=DIRECTION('',(0.,-1.,0.));
#13595=DIRECTION('center_axis',(0.,1.,0.));
#13596=DIRECTION('ref_axis',(1.,0.,0.));
#13597=DIRECTION('center_axis',(0.,1.,0.));
#13598=DIRECTION('ref_axis',(1.,0.,0.));
#13599=DIRECTION('center_axis',(0.,1.,0.));
#13600=DIRECTION('ref_axis',(1.,0.,0.));
#17155=CARTESIAN_POINT('',(0.,0.,0.));
#17156=CARTESIAN_POINT('Origin',(0.,20.85,4.81));
#17157=CARTESIAN_POINT('',(0.133884278389959,20.6882131031264,4.81));
#17158=CARTESIAN_POINT('',(0.133884278389959,21.0117868968736,4.81));
#17159=CARTESIAN_POINT('',(0.133884278389959,20.45,4.81));
#17160=CARTESIAN_POINT('Origin',(0.,20.85,4.81));
#17161=CARTESIAN_POINT('Origin',(0.,20.85,4.81));
#17162=CARTESIAN_POINT('',(-0.133884278389959,20.6882131031264,4.81));
#17163=CARTESIAN_POINT('Ctrl Pts',(-0.133884278389959,20.6882131031264,
4.81));
#17164=CARTESIAN_POINT('Ctrl Pts',(-0.118254395260803,20.6752788317824,
4.81354677224418));
#17165=CARTESIAN_POINT('Ctrl Pts',(-0.100109787682301,20.6642006834126,
4.81698224789957));
#17166=CARTESIAN_POINT('Ctrl Pts',(-0.0548298721325192,20.6453614389456,
4.8230741628997));
#17167=CARTESIAN_POINT('Ctrl Pts',(-0.0266020595922905,20.64,4.825));
#17168=CARTESIAN_POINT('Ctrl Pts',(0.0266020595922904,20.64,4.825));
#17169=CARTESIAN_POINT('Ctrl Pts',(0.0548298721325191,20.6453614389456,
4.8230741628997));
#17170=CARTESIAN_POINT('Ctrl Pts',(0.100109787682301,20.6642006834126,4.81698224789957));
#17171=CARTESIAN_POINT('Ctrl Pts',(0.118254395260803,20.6752788317824,4.81354677224418));
#17172=CARTESIAN_POINT('Ctrl Pts',(0.133884278389958,20.6882131031264,4.81));
#17173=CARTESIAN_POINT('',(-0.21,20.85,4.81));
#17174=CARTESIAN_POINT('Origin',(0.,20.85,4.81));
#17175=CARTESIAN_POINT('',(-0.21,20.85,5.29976849370594));
#17176=CARTESIAN_POINT('',(-0.21,20.85,4.81));
#17177=CARTESIAN_POINT('',(0.21,20.85,5.29976849370594));
#17178=CARTESIAN_POINT('Ctrl Pts',(0.21,20.85,5.29976849370594));
#17179=CARTESIAN_POINT('Ctrl Pts',(0.21,20.8235614118695,5.29976849370594));
#17180=CARTESIAN_POINT('Ctrl Pts',(0.204702922670976,20.7954062187451,5.30084015664674));
#17181=CARTESIAN_POINT('Ctrl Pts',(0.183251796806354,20.7436865544587,5.30468313707126));
#17182=CARTESIAN_POINT('Ctrl Pts',(0.167101177357214,20.7201163292589,5.30739593054622));
#17183=CARTESIAN_POINT('Ctrl Pts',(0.129884533480965,20.6828996853826,5.31246633289124));
#17184=CARTESIAN_POINT('Ctrl Pts',(0.106313940757288,20.6667483898366,5.31515738895358));
#17185=CARTESIAN_POINT('Ctrl Pts',(0.0545930033295199,20.6452967734303,
5.31895039220591));
#17186=CARTESIAN_POINT('Ctrl Pts',(0.0264373623835355,20.64,5.32));
#17187=CARTESIAN_POINT('Ctrl Pts',(-0.0264373623835354,20.64,5.32));
#17188=CARTESIAN_POINT('Ctrl Pts',(-0.0545930033295199,20.6452967734303,
5.31895039220591));
#17189=CARTESIAN_POINT('Ctrl Pts',(-0.106313940757288,20.6667483898366,
5.31515738895358));
#17190=CARTESIAN_POINT('Ctrl Pts',(-0.129884533480965,20.6828996853826,
5.31246633289124));
#17191=CARTESIAN_POINT('Ctrl Pts',(-0.167101177357214,20.7201163292589,
5.30739593054622));
#17192=CARTESIAN_POINT('Ctrl Pts',(-0.183251796806354,20.7436865544587,
5.30468313707126));
#17193=CARTESIAN_POINT('Ctrl Pts',(-0.204702922670976,20.7954062187451,
5.30084015664674));
#17194=CARTESIAN_POINT('Ctrl Pts',(-0.21,20.8235614118695,5.29976849370594));
#17195=CARTESIAN_POINT('Ctrl Pts',(-0.21,20.85,5.29976849370594));
#17196=CARTESIAN_POINT('Ctrl Pts',(-0.21,20.85,5.29976849370594));
#17197=CARTESIAN_POINT('Ctrl Pts',(-0.21,20.8764385881305,5.29976849370594));
#17198=CARTESIAN_POINT('Ctrl Pts',(-0.204702922670976,20.9045937812549,
5.30084015664674));
#17199=CARTESIAN_POINT('Ctrl Pts',(-0.183251796806354,20.9563134455413,
5.30468313707126));
#17200=CARTESIAN_POINT('Ctrl Pts',(-0.167101177357214,20.9798836707411,
5.30739593054622));
#17201=CARTESIAN_POINT('Ctrl Pts',(-0.129884533480965,21.0171003146174,
5.31246633289124));
#17202=CARTESIAN_POINT('Ctrl Pts',(-0.106313940757288,21.0332516101634,
5.31515738895358));
#17203=CARTESIAN_POINT('Ctrl Pts',(-0.0545930033295199,21.0547032265697,
5.31895039220591));
#17204=CARTESIAN_POINT('Ctrl Pts',(-0.0264373623835355,21.06,5.32));
#17205=CARTESIAN_POINT('Ctrl Pts',(0.0264373623835354,21.06,5.32));
#17206=CARTESIAN_POINT('Ctrl Pts',(0.0545930033295199,21.0547032265697,
5.31895039220591));
#17207=CARTESIAN_POINT('Ctrl Pts',(0.106313940757288,21.0332516101634,5.31515738895358));
#17208=CARTESIAN_POINT('Ctrl Pts',(0.129884533480965,21.0171003146174,5.31246633289124));
#17209=CARTESIAN_POINT('Ctrl Pts',(0.167101177357214,20.9798836707411,5.30739593054622));
#17210=CARTESIAN_POINT('Ctrl Pts',(0.183251796806354,20.9563134455413,5.30468313707126));
#17211=CARTESIAN_POINT('Ctrl Pts',(0.204702922670976,20.9045937812549,5.30084015664674));
#17212=CARTESIAN_POINT('Ctrl Pts',(0.21,20.8764385881305,5.29976849370594));
#17213=CARTESIAN_POINT('Ctrl Pts',(0.21,20.85,5.29976849370594));
#17214=CARTESIAN_POINT('',(-0.133884278389959,21.0117868968736,4.81));
#17215=CARTESIAN_POINT('Origin',(0.,20.85,4.81));
#17216=CARTESIAN_POINT('Ctrl Pts',(0.133884278389959,21.0117868968736,4.81));
#17217=CARTESIAN_POINT('Ctrl Pts',(0.118254395260804,21.0247211682176,4.81354677224418));
#17218=CARTESIAN_POINT('Ctrl Pts',(0.100109787682302,21.0357993165874,4.81698224789957));
#17219=CARTESIAN_POINT('Ctrl Pts',(0.0548298721325192,21.0546385610544,
4.8230741628997));
#17220=CARTESIAN_POINT('Ctrl Pts',(0.0266020595922905,21.06,4.825));
#17221=CARTESIAN_POINT('Ctrl Pts',(-0.0266020595922904,21.06,4.825));
#17222=CARTESIAN_POINT('Ctrl Pts',(-0.054829872132519,21.0546385610544,
4.8230741628997));
#17223=CARTESIAN_POINT('Ctrl Pts',(-0.100109787682301,21.0357993165874,
4.81698224789957));
#17224=CARTESIAN_POINT('Ctrl Pts',(-0.118254395260806,21.0247211682176,
4.81354677224418));
#17225=CARTESIAN_POINT('Ctrl Pts',(-0.133884278389962,21.0117868968736,
4.81));
#17226=CARTESIAN_POINT('Origin',(0.,20.85,4.81));
#17227=CARTESIAN_POINT('',(-0.133884278389959,20.45,4.81));
#17228=CARTESIAN_POINT('Origin',(0.,20.45,4.22));
#17229=CARTESIAN_POINT('',(-0.605,21.25,4.22));
#17230=CARTESIAN_POINT('Origin',(0.,21.25,4.22));
#17231=CARTESIAN_POINT('',(-0.605,20.45,4.22));
#17232=CARTESIAN_POINT('',(-0.605,20.45,4.22));
#17233=CARTESIAN_POINT('Origin',(0.,20.45,4.22));
#17234=CARTESIAN_POINT('Origin',(0.,20.45,4.22));
#17235=CARTESIAN_POINT('',(-1.1,21.25,4.22));
#17236=CARTESIAN_POINT('Origin',(0.,21.25,4.22));
#17237=CARTESIAN_POINT('',(-1.1,20.45,4.22));
#17238=CARTESIAN_POINT('',(-1.1,20.45,4.22));
#17239=CARTESIAN_POINT('Origin',(0.,20.45,4.22));
#17240=CARTESIAN_POINT('Origin',(0.,21.25,4.22));
#17241=CARTESIAN_POINT('Origin',(0.,20.45,4.22));
#19313=UNCERTAINTY_MEASURE_WITH_UNIT(LENGTH_MEASURE(0.001),#19362,
'DISTANCE_ACCURACY_VALUE',
'Maximum model space distance between geometric entities at asserted c
onnectivities');
#19323=UNCERTAINTY_MEASURE_WITH_UNIT(LENGTH_MEASURE(0.001),#19362,
'DISTANCE_ACCURACY_VALUE',
'Maximum model space distance between geometric entities at asserted c
onnectivities');
#19351=(
GEOMETRIC_REPRESENTATION_CONTEXT(3)
GLOBAL_UNCERTAINTY_ASSIGNED_CONTEXT((#19313))
GLOBAL_UNIT_ASSIGNED_CONTEXT((#19362,#19364,#19365))
REPRESENTATION_CONTEXT('','3D')
);
#19361=(
GEOMETRIC_REPRESENTATION_CONTEXT(3)
GLOBAL_UNCERTAINTY_ASSIGNED_CONTEXT((#19323))
GLOBAL_UNIT_ASSIGNED_CONTEXT((#19362,#19364,#19365))
REPRESENTATION_CONTEXT('','3D')
);
#19362=(
LENGTH_UNIT()
NAMED_UNIT(*)
SI_UNIT(.CENTI.,.METRE.)
);
#19364=(
NAMED_UNIT(*)
PLANE_ANGLE_UNIT()
SI_UNIT($,.RADIAN.)
);
#19365=(
NAMED_UNIT(*)
SI_UNIT($,.STERADIAN.)
SOLID_ANGLE_UNIT()
);
#19393=SHAPE_DEFINITION_REPRESENTATION(#19457,#19515);
#19457=PRODUCT_DEFINITION_SHAPE('',$,#19553);
#19515=SHAPE_REPRESENTATION('',(#11822),#19351);
#19525=PRODUCT_DEFINITION_CONTEXT('part definition',#19638,'design');
#19553=PRODUCT_DEFINITION('Shaft collar (1)','Shaft collar (1)',#19590,#19525);
#19590=PRODUCT_DEFINITION_FORMATION('',$,#19667);
#19638=APPLICATION_CONTEXT(
'Core Data for Automotive Mechanical Design Process');
#19639=PRODUCT_CONTEXT('part definition',#19638,'mechanical');
#19667=PRODUCT('Shaft collar (1)','Shaft collar (1)','Shaft collar (1)',(#19639));
#19740=COLOUR_RGB('Grey',0.48,0.52,0.57);
#19741=FILL_AREA_STYLE_COLOUR('',#19740);
#19742=FILL_AREA_STYLE('',(#19741));
#19743=SURFACE_STYLE_FILL_AREA(#19742);
#19744=SURFACE_SIDE_STYLE('',(#19743));
#19745=SURFACE_STYLE_USAGE(.BOTH.,#19744);
#19746=PRESENTATION_STYLE_ASSIGNMENT((#19745));
ENDSEC;
END-ISO-10303-21;
